ISO-10303-21;
HEADER;
/* Generated by software containing ST-Developer
 * from STEP Tools, Inc. (www.steptools.com) 
 */

FILE_DESCRIPTION(
/* description */ ('Pipe clamp stand with threaded column'),
/* implementation_level */ '2;1');

FILE_NAME(
/* name */ 'mm liner half (3).step',
/* time_stamp */ '2026-10-27T10:55:48-07:00',
/* author */ (''),
/* organization */ (''),
/* preprocessor_version */ 'ST-DEVELOPER v20.2',
/* originating_system */ 'Autodesk Translation Framework v15.17.0.0',
/* authorisation */ '');

FILE_SCHEMA (('AUTOMOTIVE_DESIGN { 1 0 10303 214 3 1 1 }'));
ENDSEC;

DATA;
#10=MECHANICAL_DESIGN_GEOMETRIC_PRESENTATION_REPRESENTATION('',(#760),#34433);
#708=SHAPE_REPRESENTATION_RELATIONSHIP('SRR','None',#34550,#730);
#730=ADVANCED_BREP_SHAPE_REPRESENTATION('',(#790),#34418);
#760=STYLED_ITEM('',(#34736),#790);
#790=MANIFOLD_SOLID_BREP('Body1',#8787);
#963=PLANE('',#9485);
#964=PLANE('',#9486);
#965=PLANE('',#9487);
#966=PLANE('',#9494);
#1384=FACE_OUTER_BOUND('',#1914,.T.);
#1385=FACE_OUTER_BOUND('',#1915,.T.);
#1386=FACE_OUTER_BOUND('',#1916,.T.);
#1387=FACE_OUTER_BOUND('',#1917,.T.);
#1388=FACE_OUTER_BOUND('',#1918,.T.);
#1389=FACE_OUTER_BOUND('',#1919,.T.);
#1914=EDGE_LOOP('',(#7307,#7308,#7309,#7310));
#1915=EDGE_LOOP('',(#7311,#7312,#7313,#7314));
#1916=EDGE_LOOP('',(#7315,#7316,#7317,#7318));
#1917=EDGE_LOOP('',(#7319,#7320,#7321,#7322));
#1918=EDGE_LOOP('',(#7323,#7324,#7325,#7326));
#1919=EDGE_LOOP('',(#7327,#7328,#7329,#7330));
#2499=LINE('',#28601,#3116);
#2500=LINE('',#28603,#3117);
#2501=LINE('',#28605,#3118);
#2502=LINE('',#28606,#3119);
#2503=LINE('',#28610,#3120);
#2504=LINE('',#28612,#3121);
#2505=LINE('',#28614,#3122);
#2506=LINE('',#28615,#3123);
#3116=VECTOR('',#11034,1.);
#3117=VECTOR('',#11035,1.);
#3118=VECTOR('',#11036,1.);
#3119=VECTOR('',#11037,1.);
#3120=VECTOR('',#11040,1.);
#3121=VECTOR('',#11041,1.);
#3122=VECTOR('',#11042,1.);
#3123=VECTOR('',#11043,1.);
#3400=CIRCLE('',#9488,3.1);
#3401=CIRCLE('',#9489,3.);
#3402=CIRCLE('',#9491,3.);
#3403=CIRCLE('',#9493,3.1);
#4042=VERTEX_POINT('',#28599);
#4043=VERTEX_POINT('',#28600);
#4044=VERTEX_POINT('',#28602);
#4045=VERTEX_POINT('',#28604);
#4046=VERTEX_POINT('',#28608);
#4047=VERTEX_POINT('',#28609);
#4048=VERTEX_POINT('',#28611);
#4049=VERTEX_POINT('',#28613);
#5167=EDGE_CURVE('',#4042,#4043,#2499,.T.);
#5168=EDGE_CURVE('',#4044,#4042,#2500,.T.);
#5169=EDGE_CURVE('',#4045,#4044,#2501,.T.);
#5170=EDGE_CURVE('',#4043,#4045,#2502,.T.);
#5171=EDGE_CURVE('',#4046,#4047,#2503,.T.);
#5172=EDGE_CURVE('',#4048,#4046,#2504,.T.);
#5173=EDGE_CURVE('',#4049,#4048,#2505,.T.);
#5174=EDGE_CURVE('',#4047,#4049,#2506,.T.);
#5175=EDGE_CURVE('',#4043,#4046,#3400,.T.);
#5176=EDGE_CURVE('',#4048,#4045,#3401,.T.);
#5177=EDGE_CURVE('',#4049,#4044,#3402,.T.);
#5178=EDGE_CURVE('',#4042,#4047,#3403,.T.);
#7307=ORIENTED_EDGE('',*,*,#5167,.F.);
#7308=ORIENTED_EDGE('',*,*,#5168,.F.);
#7309=ORIENTED_EDGE('',*,*,#5169,.F.);
#7310=ORIENTED_EDGE('',*,*,#5170,.F.);
#7311=ORIENTED_EDGE('',*,*,#5171,.F.);
#7312=ORIENTED_EDGE('',*,*,#5172,.F.);
#7313=ORIENTED_EDGE('',*,*,#5173,.F.);
#7314=ORIENTED_EDGE('',*,*,#5174,.F.);
#7315=ORIENTED_EDGE('',*,*,#5172,.T.);
#7316=ORIENTED_EDGE('',*,*,#5175,.F.);
#7317=ORIENTED_EDGE('',*,*,#5170,.T.);
#7318=ORIENTED_EDGE('',*,*,#5176,.F.);
#7319=ORIENTED_EDGE('',*,*,#5173,.T.);
#7320=ORIENTED_EDGE('',*,*,#5176,.T.);
#7321=ORIENTED_EDGE('',*,*,#5169,.T.);
#7322=ORIENTED_EDGE('',*,*,#5177,.F.);
#7323=ORIENTED_EDGE('',*,*,#5171,.T.);
#7324=ORIENTED_EDGE('',*,*,#5178,.F.);
#7325=ORIENTED_EDGE('',*,*,#5167,.T.);
#7326=ORIENTED_EDGE('',*,*,#5175,.T.);
#7327=ORIENTED_EDGE('',*,*,#5174,.T.);
#7328=ORIENTED_EDGE('',*,*,#5177,.T.);
#7329=ORIENTED_EDGE('',*,*,#5168,.T.);
#7330=ORIENTED_EDGE('',*,*,#5178,.T.);
#8231=CYLINDRICAL_SURFACE('',#9490,3.);
#8232=CYLINDRICAL_SURFACE('',#9492,3.1);
#8621=ADVANCED_FACE('',(#1384),#963,.F.);
#8622=ADVANCED_FACE('',(#1385),#964,.F.);
#8623=ADVANCED_FACE('',(#1386),#965,.F.);
#8624=ADVANCED_FACE('',(#1387),#8231,.F.);
#8625=ADVANCED_FACE('',(#1388),#8232,.T.);
#8626=ADVANCED_FACE('',(#1389),#966,.T.);
#8787=CLOSED_SHELL('',(#8621,#8622,#8623,#8624,#8625,#8626));
#9484=AXIS2_PLACEMENT_3D('',#28597,#11030,#11031);
#9485=AXIS2_PLACEMENT_3D('',#28598,#11032,#11033);
#9486=AXIS2_PLACEMENT_3D('',#28607,#11038,#11039);
#9487=AXIS2_PLACEMENT_3D('',#28616,#11044,#11045);
#9488=AXIS2_PLACEMENT_3D('',#28617,#11046,#11047);
#9489=AXIS2_PLACEMENT_3D('',#28618,#11048,#11049);
#9490=AXIS2_PLACEMENT_3D('',#28619,#11050,#11051);
#9491=AXIS2_PLACEMENT_3D('',#28620,#11052,#11053);
#9492=AXIS2_PLACEMENT_3D('',#28621,#11054,#11055);
#9493=AXIS2_PLACEMENT_3D('',#28622,#11056,#11057);
#9494=AXIS2_PLACEMENT_3D('',#28623,#11058,#11059);
#11030=DIRECTION('axis',(0.,0.,1.));
#11031=DIRECTION('refdir',(1.,0.,0.));
#11032=DIRECTION('center_axis',(0.,0.,1.));
#11033=DIRECTION('ref_axis',(1.,0.,0.));
#11034=DIRECTION('',(0.,-1.,0.));
#11035=DIRECTION('',(-1.,0.,0.));
#11036=DIRECTION('',(0.,1.,0.));
#11037=DIRECTION('',(1.,0.,0.));
#11038=DIRECTION('center_axis',(0.,0.,1.));
#11039=DIRECTION('ref_axis',(1.,0.,0.));
#11040=DIRECTION('',(0.,1.,0.));
#11041=DIRECTION('',(1.,0.,0.));
#11042=DIRECTION('',(0.,-1.,0.));
#11043=DIRECTION('',(-1.,0.,0.));
#11044=DIRECTION('center_axis',(0.,1.,0.));
#11045=DIRECTION('ref_axis',(1.,0.,0.));
#11046=DIRECTION('center_axis',(0.,1.,0.));
#11047=DIRECTION('ref_axis',(1.,0.,0.));
#11048=DIRECTION('center_axis',(0.,-1.,0.));
#11049=DIRECTION('ref_axis',(1.,0.,0.));
#11050=DIRECTION('center_axis',(0.,1.,0.));
#11051=DIRECTION('ref_axis',(1.,0.,0.));
#11052=DIRECTION('center_axis',(0.,-1.,0.));
#11053=DIRECTION('ref_axis',(1.,0.,0.));
#11054=DIRECTION('center_axis',(0.,1.,0.));
#11055=DIRECTION('ref_axis',(1.,0.,0.));
#11056=DIRECTION('center_axis',(0.,1.,0.));
#11057=DIRECTION('ref_axis',(1.,0.,0.));
#11058=DIRECTION('center_axis',(0.,1.,0.));
#11059=DIRECTION('ref_axis',(1.,0.,0.));
#28597=CARTESIAN_POINT('',(0.,0.,0.));
#28598=CARTESIAN_POINT('Origin',(-8.4,-1.1,28.025));
#28599=CARTESIAN_POINT('',(-3.09989919190931,1.,28.025));
#28600=CARTESIAN_POINT('',(-3.09989919190931,-1.,28.025));
#28601=CARTESIAN_POINT('',(-3.09989919190931,-1.,28.025));
#28602=CARTESIAN_POINT('',(-2.99989583152482,1.,28.025));
#28603=CARTESIAN_POINT('',(-4.2,1.,28.025));
#28604=CARTESIAN_POINT('',(-2.99989583152482,-1.,28.025));
#28605=CARTESIAN_POINT('',(-2.99989583152482,-1.,28.025));
#28606=CARTESIAN_POINT('',(-4.2,-1.,28.025));
#28607=CARTESIAN_POINT('Origin',(-8.4,-1.1,28.025));
#28608=CARTESIAN_POINT('',(3.09989919190931,-1.,28.025));
#28609=CARTESIAN_POINT('',(3.09989919190931,1.,28.025));
#28610=CARTESIAN_POINT('',(3.09989919190931,-1.,28.025));
#28611=CARTESIAN_POINT('',(2.99989583152482,-1.,28.025));
#28612=CARTESIAN_POINT('',(-4.2,-1.,28.025));
#28613=CARTESIAN_POINT('',(2.99989583152482,1.,28.025));
#28614=CARTESIAN_POINT('',(2.99989583152482,-1.,28.025));
#28615=CARTESIAN_POINT('',(-4.2,1.,28.025));
#28616=CARTESIAN_POINT('Origin',(0.,-1.,28.));
#28617=CARTESIAN_POINT('Origin',(0.,-1.,28.));
#28618=CARTESIAN_POINT('Origin',(0.,-1.,28.));
#28619=CARTESIAN_POINT('Origin',(0.,-1.,28.));
#28620=CARTESIAN_POINT('Origin',(0.,1.,28.));
#28621=CARTESIAN_POINT('Origin',(0.,-1.,28.));
#28622=CARTESIAN_POINT('Origin',(0.,1.,28.));
#28623=CARTESIAN_POINT('Origin',(0.,1.,28.));
#34389=UNCERTAINTY_MEASURE_WITH_UNIT(LENGTH_MEASURE(0.001),#34434,
'DISTANCE_ACCURACY_VALUE',
'Maximum model space distance between geometric entities at asserted c
onnectivities');
#34404=UNCERTAINTY_MEASURE_WITH_UNIT(LENGTH_MEASURE(0.001),#34434,
'DISTANCE_ACCURACY_VALUE',
'Maximum model space distance between geometric entities at asserted c
onnectivities');
#34418=(
GEOMETRIC_REPRESENTATION_CONTEXT(3)
GLOBAL_UNCERTAINTY_ASSIGNED_CONTEXT((#34389))
GLOBAL_UNIT_ASSIGNED_CONTEXT((#34434,#34436,#34437))
REPRESENTATION_CONTEXT('','3D')
);
#34433=(
GEOMETRIC_REPRESENTATION_CONTEXT(3)
GLOBAL_UNCERTAINTY_ASSIGNED_CONTEXT((#34404))
GLOBAL_UNIT_ASSIGNED_CONTEXT((#34434,#34436,#34437))
REPRESENTATION_CONTEXT('','3D')
);
#34434=(
LENGTH_UNIT()
NAMED_UNIT(*)
SI_UNIT(.CENTI.,.METRE.)
);
#34436=(
NAMED_UNIT(*)
PLANE_ANGLE_UNIT()
SI_UNIT($,.RADIAN.)
);
#34437=(
NAMED_UNIT(*)
SI_UNIT($,.STERADIAN.)
SOLID_ANGLE_UNIT()
);
#34451=SHAPE_DEFINITION_REPRESENTATION(#34479,#34550);
#34479=PRODUCT_DEFINITION_SHAPE('',$,#34579);
#34550=SHAPE_REPRESENTATION('',(#9484),#34418);
#34565=PRODUCT_DEFINITION_CONTEXT('part definition',#34651,'design');
#34579=PRODUCT_DEFINITION('mm liner half (3)','mm liner half (3)',#34607,
#34565);
#34607=PRODUCT_DEFINITION_FORMATION('',$,#34666);
#34651=APPLICATION_CONTEXT(
'Core Data for Automotive Mechanical Design Process');
#34652=PRODUCT_CONTEXT('part definition',#34651,'mechanical');
#34666=PRODUCT('mm liner half (3)','mm liner half (3)','mm liner half (3)',(#34652));
#34730=COLOUR_RGB('Sky Blue',0.24,0.69,0.87);
#34731=FILL_AREA_STYLE_COLOUR('',#34730);
#34732=FILL_AREA_STYLE('',(#34731));
#34733=SURFACE_STYLE_FILL_AREA(#34732);
#34734=SURFACE_SIDE_STYLE('',(#34733));
#34735=SURFACE_STYLE_USAGE(.BOTH.,#34734);
#34736=PRESENTATION_STYLE_ASSIGNMENT((#34735));
ENDSEC;
END-ISO-10303-21;
